ISO-10303-21;
HEADER;
/* Generated by software containing ST-Developer
 * from STEP Tools, Inc. (www.steptools.com) 
 */

FILE_DESCRIPTION(
/* description */ ('Bell-crank linkage with push rods'),
/* implementation_level */ '2;1');

FILE_NAME(
/* name */ 'Plain link bushing (1).step',
/* time_stamp */ '2026-10-28T03:25:15-07:00',
/* author */ (''),
/* organization */ (''),
/* preprocessor_version */ 'ST-DEVELOPER v20.2',
/* originating_system */ 'Autodesk Translation Framework v15.17.0.0',
/* authorisation */ '');

FILE_SCHEMA (('AUTOMOTIVE_DESIGN { 1 0 10303 214 3 1 1 }'));
ENDSEC;

DATA;
#10=MECHANICAL_DESIGN_GEOMETRIC_PRESENTATION_REPRESENTATION('',(#645),#16678);
#529=SHAPE_REPRESENTATION_RELATIONSHIP('SRR','None',#16948,#583);
#583=ADVANCED_BREP_SHAPE_REPRESENTATION('',(#705),#16653);
#645=STYLED_ITEM('',(#17284),#705);
#705=MANIFOLD_SOLID_BREP('Body1',#8837);
#864=FACE_BOUND('',#2260,.T.);
#865=FACE_BOUND('',#2262,.T.);
#1149=PLANE('',#10190);
#1150=PLANE('',#10191);
#1596=FACE_OUTER_BOUND('',#2257,.T.);
#1597=FACE_OUTER_BOUND('',#2258,.T.);
#1598=FACE_OUTER_BOUND('',#2259,.T.);
#1599=FACE_OUTER_BOUND('',#2261,.T.);
#2257=EDGE_LOOP('',(#7383,#7384,#7385,#7386));
#2258=EDGE_LOOP('',(#7387,#7388,#7389,#7390));
#2259=EDGE_LOOP('',(#7391));
#2260=EDGE_LOOP('',(#7392));
#2261=EDGE_LOOP('',(#7393));
#2262=EDGE_LOOP('',(#7394));
#2892=LINE('',#15693,#3441);
#2893=LINE('',#15699,#3442);
#3441=VECTOR('',#12454,0.305);
#3442=VECTOR('',#12461,0.5);
#3967=CIRCLE('',#10185,0.305);
#3968=CIRCLE('',#10186,0.305);
#3969=CIRCLE('',#10188,0.5);
#3970=CIRCLE('',#10189,0.5);
#4606=VERTEX_POINT('',#15690);
#4607=VERTEX_POINT('',#15692);
#4608=VERTEX_POINT('',#15696);
#4609=VERTEX_POINT('',#15698);
#5569=EDGE_CURVE('',#4606,#4606,#3967,.T.);
#5570=EDGE_CURVE('',#4606,#4607,#2892,.T.);
#5571=EDGE_CURVE('',#4607,#4607,#3968,.T.);
#5572=EDGE_CURVE('',#4608,#4608,#3969,.T.);
#5573=EDGE_CURVE('',#4608,#4609,#2893,.T.);
#5574=EDGE_CURVE('',#4609,#4609,#3970,.T.);
#7383=ORIENTED_EDGE('',*,*,#5569,.F.);
#7384=ORIENTED_EDGE('',*,*,#5570,.T.);
#7385=ORIENTED_EDGE('',*,*,#5571,.T.);
#7386=ORIENTED_EDGE('',*,*,#5570,.F.);
#7387=ORIENTED_EDGE('',*,*,#5572,.F.);
#7388=ORIENTED_EDGE('',*,*,#5573,.T.);
#7389=ORIENTED_EDGE('',*,*,#5574,.T.);
#7390=ORIENTED_EDGE('',*,*,#5573,.F.);
#7391=ORIENTED_EDGE('',*,*,#5572,.T.);
#7392=ORIENTED_EDGE('',*,*,#5569,.T.);
#7393=ORIENTED_EDGE('',*,*,#5574,.F.);
#7394=ORIENTED_EDGE('',*,*,#5571,.F.);
#8200=CYLINDRICAL_SURFACE('',#10184,0.305);
#8201=CYLINDRICAL_SURFACE('',#10187,0.5);
#8621=ADVANCED_FACE('',(#1596),#8200,.F.);
#8622=ADVANCED_FACE('',(#1597),#8201,.T.);
#8623=ADVANCED_FACE('',(#1598,#864),#1149,.T.);
#8624=ADVANCED_FACE('',(#1599,#865),#1150,.F.);
#8837=CLOSED_SHELL('',(#8621,#8622,#8623,#8624));
#10183=AXIS2_PLACEMENT_3D('',#15688,#12448,#12449);
#10184=AXIS2_PLACEMENT_3D('',#15689,#12450,#12451);
#10185=AXIS2_PLACEMENT_3D('',#15691,#12452,#12453);
#10186=AXIS2_PLACEMENT_3D('',#15694,#12455,#12456);
#10187=AXIS2_PLACEMENT_3D('',#15695,#12457,#12458);
#10188=AXIS2_PLACEMENT_3D('',#15697,#12459,#12460);
#10189=AXIS2_PLACEMENT_3D('',#15700,#12462,#12463);
#10190=AXIS2_PLACEMENT_3D('',#15701,#12464,#12465);
#10191=AXIS2_PLACEMENT_3D('',#15702,#12466,#12467);
#12448=DIRECTION('axis',(0.,0.,1.));
#12449=DIRECTION('refdir',(1.,0.,0.));
#12450=DIRECTION('center_axis',(0.,0.,1.));
#12451=DIRECTION('ref_axis',(1.,0.,0.));
#12452=DIRECTION('center_axis',(0.,0.,-1.));
#12453=DIRECTION('ref_axis',(1.,0.,0.));
#12454=DIRECTION('',(0.,0.,-1.));
#12455=DIRECTION('center_axis',(0.,0.,-1.));
#12456=DIRECTION('ref_axis',(1.,0.,0.));
#12457=DIRECTION('center_axis',(0.,0.,1.));
#12458=DIRECTION('ref_axis',(1.,0.,0.));
#12459=DIRECTION('center_axis',(0.,0.,1.));
#12460=DIRECTION('ref_axis',(1.,0.,0.));
#12461=DIRECTION('',(0.,0.,-1.));
#12462=DIRECTION('center_axis',(0.,0.,1.));
#12463=DIRECTION('ref_axis',(1.,0.,0.));
#12464=DIRECTION('center_axis',(0.,0.,1.));
#12465=DIRECTION('ref_axis',(1.,0.,0.));
#12466=DIRECTION('center_axis',(0.,0.,1.));
#12467=DIRECTION('ref_axis',(1.,0.,0.));
#15688=CARTESIAN_POINT('',(0.,0.,0.));
#15689=CARTESIAN_POINT('Origin',(10.,2.,8.8));
#15690=CARTESIAN_POINT('',(9.695,2.,9.6));
#15691=CARTESIAN_POINT('Origin',(10.,2.,9.6));
#15692=CARTESIAN_POINT('',(9.695,2.,8.8));
#15693=CARTESIAN_POINT('',(9.695,2.,8.8));
#15694=CARTESIAN_POINT('Origin',(10.,2.,8.8));
#15695=CARTESIAN_POINT('Origin',(10.,2.,8.8));
#15696=CARTESIAN_POINT('',(9.5,2.,9.6));
#15697=CARTESIAN_POINT('Origin',(10.,2.,9.6));
#15698=CARTESIAN_POINT('',(9.5,2.,8.8));
#15699=CARTESIAN_POINT('',(9.5,2.,8.8));
#15700=CARTESIAN_POINT('Origin',(10.,2.,8.8));
#15701=CARTESIAN_POINT('Origin',(10.,2.,9.6));
#15702=CARTESIAN_POINT('Origin',(10.,2.,8.8));
#16589=UNCERTAINTY_MEASURE_WITH_UNIT(LENGTH_MEASURE(0.001),#16679,
'DISTANCE_ACCURACY_VALUE',
'Maximum model space distance between geometric entities at asserted c
onnectivities');
#16614=UNCERTAINTY_MEASURE_WITH_UNIT(LENGTH_MEASURE(0.001),#16679,
'DISTANCE_ACCURACY_VALUE',
'Maximum model space distance between geometric entities at asserted c
onnectivities');
#16653=(
GEOMETRIC_REPRESENTATION_CONTEXT(3)
GLOBAL_UNCERTAINTY_ASSIGNED_CONTEXT((#16589))
GLOBAL_UNIT_ASSIGNED_CONTEXT((#16679,#16681,#16682))
REPRESENTATION_CONTEXT('','3D')
);
#16678=(
GEOMETRIC_REPRESENTATION_CONTEXT(3)
GLOBAL_UNCERTAINTY_ASSIGNED_CONTEXT((#16614))
GLOBAL_UNIT_ASSIGNED_CONTEXT((#16679,#16681,#16682))
REPRESENTATION_CONTEXT('','3D')
);
#16679=(
LENGTH_UNIT()
NAMED_UNIT(*)
SI_UNIT(.CENTI.,.METRE.)
);
#16681=(
NAMED_UNIT(*)
PLANE_ANGLE_UNIT()
SI_UNIT($,.RADIAN.)
);
#16682=(
NAMED_UNIT(*)
SI_UNIT($,.STERADIAN.)
SOLID_ANGLE_UNIT()
);
#16721=SHAPE_DEFINITION_REPRESENTATION(#16789,#16948);
#16789=PRODUCT_DEFINITION_SHAPE('',$,#17012);
#16948=SHAPE_REPRESENTATION('',(#10183),#16653);
#16973=PRODUCT_DEFINITION_CONTEXT('part definition',#17164,'design');
#17012=PRODUCT_DEFINITION('Plain link bushing (1)',
'Plain link bushing (1)',#17075,#16973);
#17075=PRODUCT_DEFINITION_FORMATION('',$,#17204);
#17164=APPLICATION_CONTEXT(
'Core Data for Automotive Mechanical Design Process');
#17165=PRODUCT_CONTEXT('part definition',#17164,'mechanical');
#17204=PRODUCT('Plain link bushing (1)','Plain link bushing (1)',
'Plain link bushing (1)',(#17165));
#17278=COLOUR_RGB('Sky Blue',0.24,0.69,0.87);
#17279=FILL_AREA_STYLE_COLOUR('',#17278);
#17280=FILL_AREA_STYLE('',(#17279));
#17281=SURFACE_STYLE_FILL_AREA(#17280);
#17282=SURFACE_SIDE_STYLE('',(#17281));
#17283=SURFACE_STYLE_USAGE(.BOTH.,#17282);
#17284=PRESENTATION_STYLE_ASSIGNMENT((#17283));
ENDSEC;
END-ISO-10303-21;
